ISO-10303-21;
HEADER;
/* Generated by software containing ST-Developer
 * from STEP Tools, Inc. (www.steptools.com) 
 */

FILE_DESCRIPTION(
/* description */ (''),
/* implementation_level */ '2;1');

FILE_NAME(
/* name */ '09_Circlip_DIN_472_-_28.step',
/* time_stamp */ '2026-10-26T06:59:52-07:00',
/* author */ (''),
/* organization */ (''),
/* preprocessor_version */ 'ST-DEVELOPER v20.2',
/* originating_system */ 'Autodesk Translation Framework v15.15.0.0',
/* authorisation */ '');

FILE_SCHEMA (('AUTOMOTIVE_DESIGN { 1 0 10303 214 3 1 1 }'));
ENDSEC;

DATA;
#10=MECHANICAL_DESIGN_GEOMETRIC_PRESENTATION_REPRESENTATION('',(#171),#46395);
#111=ELLIPSE('',#26459,20.7889393668845,14.7);
#112=ELLIPSE('',#26464,20.7889393668845,14.7);
#113=ELLIPSE('',#26470,20.7889393668845,14.7);
#114=ELLIPSE('',#26474,20.7889393668845,14.7);
#143=SHAPE_REPRESENTATION_RELATIONSHIP('SRR','None',#46463,#157);
#157=ADVANCED_BREP_SHAPE_REPRESENTATION('',(#185),#46388);
#171=STYLED_ITEM('',(#46596),#185);
#185=MANIFOLD_SOLID_BREP('Body1',#24944);
#297=B_SPLINE_CURVE_WITH_KNOTS('',3,(#40254,#40255,#40256,#40257),
 .UNSPECIFIED.,.F.,.F.,(4,4),(0.,0.0322321858890298),.UNSPECIFIED.);
#298=B_SPLINE_CURVE_WITH_KNOTS('',3,(#40263,#40264,#40265,#40266),
 .UNSPECIFIED.,.F.,.F.,(4,4),(0.,0.0322321858888913),.UNSPECIFIED.);
#299=B_SPLINE_CURVE_WITH_KNOTS('',3,(#40292,#40293,#40294,#40295),
 .UNSPECIFIED.,.F.,.F.,(4,4),(0.,0.0322321858888547),.UNSPECIFIED.);
#300=B_SPLINE_CURVE_WITH_KNOTS('',3,(#40299,#40300,#40301,#40302),
 .UNSPECIFIED.,.F.,.F.,(4,4),(0.,0.0322321858887643),.UNSPECIFIED.);
#526=CYLINDRICAL_SURFACE('',#26466,12.2);
#527=CYLINDRICAL_SURFACE('',#26479,14.7);
#528=CYLINDRICAL_SURFACE('',#26483,0.800000000000001);
#529=CYLINDRICAL_SURFACE('',#26491,0.800000000000001);
#661=FACE_BOUND('',#4186,.T.);
#662=FACE_BOUND('',#4187,.T.);
#663=FACE_BOUND('',#4193,.T.);
#664=FACE_BOUND('',#4194,.T.);
#1516=PLANE('',#26458);
#1517=PLANE('',#26463);
#1518=PLANE('',#26465);
#1519=PLANE('',#26468);
#1520=PLANE('',#26469);
#1521=PLANE('',#26473);
#1522=PLANE('',#26475);
#1523=PLANE('',#26487);
#2770=FACE_OUTER_BOUND('',#4176,.T.);
#2771=FACE_OUTER_BOUND('',#4177,.T.);
#2772=FACE_OUTER_BOUND('',#4178,.T.);
#2773=FACE_OUTER_BOUND('',#4179,.T.);
#2774=FACE_OUTER_BOUND('',#4180,.T.);
#2775=FACE_OUTER_BOUND('',#4181,.T.);
#2776=FACE_OUTER_BOUND('',#4182,.T.);
#2777=FACE_OUTER_BOUND('',#4183,.T.);
#2778=FACE_OUTER_BOUND('',#4184,.T.);
#2779=FACE_OUTER_BOUND('',#4185,.T.);
#2780=FACE_OUTER_BOUND('',#4188,.T.);
#2781=FACE_OUTER_BOUND('',#4189,.T.);
#2782=FACE_OUTER_BOUND('',#4190,.T.);
#2783=FACE_OUTER_BOUND('',#4191,.T.);
#2784=FACE_OUTER_BOUND('',#4192,.T.);
#2785=FACE_OUTER_BOUND('',#4195,.T.);
#2786=FACE_OUTER_BOUND('',#4196,.T.);
#2787=FACE_OUTER_BOUND('',#4197,.T.);
#4176=EDGE_LOOP('',(#22122,#22123,#22124,#22125));
#4177=EDGE_LOOP('',(#22126,#22127,#22128,#22129));
#4178=EDGE_LOOP('',(#22130,#22131,#22132,#22133));
#4179=EDGE_LOOP('',(#22134,#22135,#22136,#22137));
#4180=EDGE_LOOP('',(#22138,#22139,#22140,#22141));
#4181=EDGE_LOOP('',(#22142,#22143,#22144,#22145));
#4182=EDGE_LOOP('',(#22146,#22147,#22148,#22149));
#4183=EDGE_LOOP('',(#22150,#22151,#22152,#22153));
#4184=EDGE_LOOP('',(#22154,#22155,#22156,#22157));
#4185=EDGE_LOOP('',(#22158,#22159,#22160,#22161));
#4186=EDGE_LOOP('',(#22162));
#4187=EDGE_LOOP('',(#22163));
#4188=EDGE_LOOP('',(#22164,#22165,#22166,#22167,#22168,#22169,#22170,#22171));
#4189=EDGE_LOOP('',(#22172,#22173,#22174,#22175));
#4190=EDGE_LOOP('',(#22176,#22177,#22178,#22179));
#4191=EDGE_LOOP('',(#22180,#22181,#22182,#22183));
#4192=EDGE_LOOP('',(#22184,#22185,#22186,#22187));
#4193=EDGE_LOOP('',(#22188));
#4194=EDGE_LOOP('',(#22189));
#4195=EDGE_LOOP('',(#22190,#22191,#22192,#22193));
#4196=EDGE_LOOP('',(#22194,#22195,#22196,#22197));
#4197=EDGE_LOOP('',(#22198,#22199,#22200,#22201));
#6933=LINE('',#40249,#9802);
#6934=LINE('',#40253,#9803);
#6935=LINE('',#40269,#9804);
#6936=LINE('',#40272,#9805);
#6937=LINE('',#40275,#9806);
#6938=LINE('',#40277,#9807);
#6939=LINE('',#40278,#9808);
#6940=LINE('',#40281,#9809);
#6941=LINE('',#40285,#9810);
#6942=LINE('',#40286,#9811);
#6943=LINE('',#40291,#9812);
#6944=LINE('',#40305,#9813);
#6945=LINE('',#40317,#9814);
#6946=LINE('',#40321,#9815);
#6947=LINE('',#40326,#9816);
#6948=LINE('',#40332,#9817);
#6949=LINE('',#40336,#9818);
#6950=LINE('',#40339,#9819);
#9802=VECTOR('',#32038,10.);
#9803=VECTOR('',#32041,10.);
#9804=VECTOR('',#32050,10.);
#9805=VECTOR('',#32053,10.);
#9806=VECTOR('',#32056,10.);
#9807=VECTOR('',#32057,10.);
#9808=VECTOR('',#32058,10.);
#9809=VECTOR('',#32061,10.);
#9810=VECTOR('',#32066,10.);
#9811=VECTOR('',#32067,10.);
#9812=VECTOR('',#32072,10.);
#9813=VECTOR('',#32079,10.);
#9814=VECTOR('',#32096,0.900000000000001);
#9815=VECTOR('',#32101,0.800000000000001);
#9816=VECTOR('',#32108,0.900000000000001);
#9817=VECTOR('',#32115,0.900000000000001);
#9818=VECTOR('',#32120,0.800000000000001);
#9819=VECTOR('',#32125,0.900000000000001);
#10600=CIRCLE('',#26461,12.2);
#10601=CIRCLE('',#26462,12.4);
#10602=CIRCLE('',#26467,12.2);
#10603=CIRCLE('',#26472,12.4);
#10604=CIRCLE('',#26476,14.7);
#10605=CIRCLE('',#26477,1.);
#10606=CIRCLE('',#26478,1.);
#10607=CIRCLE('',#26480,14.7);
#10608=CIRCLE('',#26482,0.800000000000001);
#10609=CIRCLE('',#26484,0.800000000000001);
#10610=CIRCLE('',#26486,1.);
#10611=CIRCLE('',#26488,1.);
#10612=CIRCLE('',#26490,0.800000000000001);
#10613=CIRCLE('',#26492,0.800000000000001);
#12555=VERTEX_POINT('',#40247);
#12556=VERTEX_POINT('',#40248);
#12557=VERTEX_POINT('',#40250);
#12558=VERTEX_POINT('',#40252);
#12559=VERTEX_POINT('',#40259);
#12560=VERTEX_POINT('',#40261);
#12561=VERTEX_POINT('',#40268);
#12562=VERTEX_POINT('',#40270);
#12563=VERTEX_POINT('',#40274);
#12564=VERTEX_POINT('',#40276);
#12565=VERTEX_POINT('',#40280);
#12566=VERTEX_POINT('',#40284);
#12567=VERTEX_POINT('',#40288);
#12568=VERTEX_POINT('',#40290);
#12569=VERTEX_POINT('',#40297);
#12570=VERTEX_POINT('',#40304);
#12571=VERTEX_POINT('',#40309);
#12572=VERTEX_POINT('',#40311);
#12573=VERTEX_POINT('',#40316);
#12574=VERTEX_POINT('',#40320);
#12575=VERTEX_POINT('',#40324);
#12576=VERTEX_POINT('',#40328);
#12577=VERTEX_POINT('',#40331);
#12578=VERTEX_POINT('',#40335);
#15814=EDGE_CURVE('',#12555,#12556,#6933,.T.);
#15815=EDGE_CURVE('',#12556,#12557,#111,.T.);
#15816=EDGE_CURVE('',#12557,#12558,#6934,.T.);
#15817=EDGE_CURVE('',#12558,#12555,#297,.T.);
#15818=EDGE_CURVE('',#12559,#12555,#10600,.T.);
#15819=EDGE_CURVE('',#12558,#12560,#10601,.T.);
#15820=EDGE_CURVE('',#12560,#12559,#298,.T.);
#15821=EDGE_CURVE('',#12560,#12561,#6935,.T.);
#15822=EDGE_CURVE('',#12561,#12562,#112,.T.);
#15823=EDGE_CURVE('',#12562,#12559,#6936,.T.);
#15824=EDGE_CURVE('',#12563,#12555,#6937,.T.);
#15825=EDGE_CURVE('',#12564,#12563,#6938,.T.);
#15826=EDGE_CURVE('',#12564,#12556,#6939,.T.);
#15827=EDGE_CURVE('',#12565,#12559,#6940,.T.);
#15828=EDGE_CURVE('',#12563,#12565,#10602,.T.);
#15829=EDGE_CURVE('',#12566,#12562,#6941,.T.);
#15830=EDGE_CURVE('',#12565,#12566,#6942,.T.);
#15831=EDGE_CURVE('',#12566,#12567,#113,.T.);
#15832=EDGE_CURVE('',#12567,#12568,#6943,.T.);
#15833=EDGE_CURVE('',#12568,#12565,#299,.T.);
#15834=EDGE_CURVE('',#12568,#12569,#10603,.T.);
#15835=EDGE_CURVE('',#12569,#12563,#300,.T.);
#15836=EDGE_CURVE('',#12569,#12570,#6944,.T.);
#15837=EDGE_CURVE('',#12570,#12564,#114,.T.);
#15838=EDGE_CURVE('',#12570,#12567,#10604,.T.);
#15839=EDGE_CURVE('',#12571,#12571,#10605,.T.);
#15840=EDGE_CURVE('',#12572,#12572,#10606,.T.);
#15841=EDGE_CURVE('',#12557,#12561,#10607,.T.);
#15842=EDGE_CURVE('',#12571,#12573,#6945,.T.);
#15843=EDGE_CURVE('',#12573,#12573,#10608,.T.);
#15844=EDGE_CURVE('',#12573,#12574,#6946,.T.);
#15845=EDGE_CURVE('',#12574,#12574,#10609,.T.);
#15846=EDGE_CURVE('',#12575,#12575,#10610,.T.);
#15847=EDGE_CURVE('',#12575,#12574,#6947,.T.);
#15848=EDGE_CURVE('',#12576,#12576,#10611,.T.);
#15849=EDGE_CURVE('',#12572,#12577,#6948,.T.);
#15850=EDGE_CURVE('',#12577,#12577,#10612,.T.);
#15851=EDGE_CURVE('',#12577,#12578,#6949,.T.);
#15852=EDGE_CURVE('',#12578,#12578,#10613,.T.);
#15853=EDGE_CURVE('',#12576,#12578,#6950,.T.);
#22122=ORIENTED_EDGE('',*,*,#15814,.T.);
#22123=ORIENTED_EDGE('',*,*,#15815,.T.);
#22124=ORIENTED_EDGE('',*,*,#15816,.T.);
#22125=ORIENTED_EDGE('',*,*,#15817,.T.);
#22126=ORIENTED_EDGE('',*,*,#15818,.T.);
#22127=ORIENTED_EDGE('',*,*,#15817,.F.);
#22128=ORIENTED_EDGE('',*,*,#15819,.T.);
#22129=ORIENTED_EDGE('',*,*,#15820,.T.);
#22130=ORIENTED_EDGE('',*,*,#15821,.T.);
#22131=ORIENTED_EDGE('',*,*,#15822,.T.);
#22132=ORIENTED_EDGE('',*,*,#15823,.T.);
#22133=ORIENTED_EDGE('',*,*,#15820,.F.);
#22134=ORIENTED_EDGE('',*,*,#15814,.F.);
#22135=ORIENTED_EDGE('',*,*,#15824,.F.);
#22136=ORIENTED_EDGE('',*,*,#15825,.F.);
#22137=ORIENTED_EDGE('',*,*,#15826,.T.);
#22138=ORIENTED_EDGE('',*,*,#15818,.F.);
#22139=ORIENTED_EDGE('',*,*,#15827,.F.);
#22140=ORIENTED_EDGE('',*,*,#15828,.F.);
#22141=ORIENTED_EDGE('',*,*,#15824,.T.);
#22142=ORIENTED_EDGE('',*,*,#15823,.F.);
#22143=ORIENTED_EDGE('',*,*,#15829,.F.);
#22144=ORIENTED_EDGE('',*,*,#15830,.F.);
#22145=ORIENTED_EDGE('',*,*,#15827,.T.);
#22146=ORIENTED_EDGE('',*,*,#15830,.T.);
#22147=ORIENTED_EDGE('',*,*,#15831,.T.);
#22148=ORIENTED_EDGE('',*,*,#15832,.T.);
#22149=ORIENTED_EDGE('',*,*,#15833,.T.);
#22150=ORIENTED_EDGE('',*,*,#15834,.T.);
#22151=ORIENTED_EDGE('',*,*,#15835,.T.);
#22152=ORIENTED_EDGE('',*,*,#15828,.T.);
#22153=ORIENTED_EDGE('',*,*,#15833,.F.);
#22154=ORIENTED_EDGE('',*,*,#15836,.T.);
#22155=ORIENTED_EDGE('',*,*,#15837,.T.);
#22156=ORIENTED_EDGE('',*,*,#15825,.T.);
#22157=ORIENTED_EDGE('',*,*,#15835,.F.);
#22158=ORIENTED_EDGE('',*,*,#15836,.F.);
#22159=ORIENTED_EDGE('',*,*,#15834,.F.);
#22160=ORIENTED_EDGE('',*,*,#15832,.F.);
#22161=ORIENTED_EDGE('',*,*,#15838,.F.);
#22162=ORIENTED_EDGE('',*,*,#15839,.F.);
#22163=ORIENTED_EDGE('',*,*,#15840,.F.);
#22164=ORIENTED_EDGE('',*,*,#15815,.F.);
#22165=ORIENTED_EDGE('',*,*,#15826,.F.);
#22166=ORIENTED_EDGE('',*,*,#15837,.F.);
#22167=ORIENTED_EDGE('',*,*,#15838,.T.);
#22168=ORIENTED_EDGE('',*,*,#15831,.F.);
#22169=ORIENTED_EDGE('',*,*,#15829,.T.);
#22170=ORIENTED_EDGE('',*,*,#15822,.F.);
#22171=ORIENTED_EDGE('',*,*,#15841,.F.);
#22172=ORIENTED_EDGE('',*,*,#15839,.T.);
#22173=ORIENTED_EDGE('',*,*,#15842,.T.);
#22174=ORIENTED_EDGE('',*,*,#15843,.T.);
#22175=ORIENTED_EDGE('',*,*,#15842,.F.);
#22176=ORIENTED_EDGE('',*,*,#15843,.F.);
#22177=ORIENTED_EDGE('',*,*,#15844,.T.);
#22178=ORIENTED_EDGE('',*,*,#15845,.F.);
#22179=ORIENTED_EDGE('',*,*,#15844,.F.);
#22180=ORIENTED_EDGE('',*,*,#15846,.T.);
#22181=ORIENTED_EDGE('',*,*,#15847,.T.);
#22182=ORIENTED_EDGE('',*,*,#15845,.T.);
#22183=ORIENTED_EDGE('',*,*,#15847,.F.);
#22184=ORIENTED_EDGE('',*,*,#15816,.F.);
#22185=ORIENTED_EDGE('',*,*,#15841,.T.);
#22186=ORIENTED_EDGE('',*,*,#15821,.F.);
#22187=ORIENTED_EDGE('',*,*,#15819,.F.);
#22188=ORIENTED_EDGE('',*,*,#15848,.F.);
#22189=ORIENTED_EDGE('',*,*,#15846,.F.);
#22190=ORIENTED_EDGE('',*,*,#15840,.T.);
#22191=ORIENTED_EDGE('',*,*,#15849,.T.);
#22192=ORIENTED_EDGE('',*,*,#15850,.T.);
#22193=ORIENTED_EDGE('',*,*,#15849,.F.);
#22194=ORIENTED_EDGE('',*,*,#15850,.F.);
#22195=ORIENTED_EDGE('',*,*,#15851,.T.);
#22196=ORIENTED_EDGE('',*,*,#15852,.F.);
#22197=ORIENTED_EDGE('',*,*,#15851,.F.);
#22198=ORIENTED_EDGE('',*,*,#15848,.T.);
#22199=ORIENTED_EDGE('',*,*,#15853,.T.);
#22200=ORIENTED_EDGE('',*,*,#15852,.T.);
#22201=ORIENTED_EDGE('',*,*,#15853,.F.);
#23593=CONICAL_SURFACE('',#26460,12.3,0.785398163397449);
#23594=CONICAL_SURFACE('',#26471,12.3,0.785398163397449);
#23595=CONICAL_SURFACE('',#26481,0.900000000000001,0.785398163397449);
#23596=CONICAL_SURFACE('',#26485,0.900000000000001,0.785398163397449);
#23597=CONICAL_SURFACE('',#26489,0.900000000000001,0.785398163397449);
#23598=CONICAL_SURFACE('',#26493,0.900000000000001,0.785398163397449);
#24629=ADVANCED_FACE('',(#2770),#1516,.T.);
#24630=ADVANCED_FACE('',(#2771),#23593,.F.);
#24631=ADVANCED_FACE('',(#2772),#1517,.T.);
#24632=ADVANCED_FACE('',(#2773),#1518,.T.);
#24633=ADVANCED_FACE('',(#2774),#526,.F.);
#24634=ADVANCED_FACE('',(#2775),#1519,.T.);
#24635=ADVANCED_FACE('',(#2776),#1520,.T.);
#24636=ADVANCED_FACE('',(#2777),#23594,.F.);
#24637=ADVANCED_FACE('',(#2778),#1521,.T.);
#24638=ADVANCED_FACE('',(#2779,#661,#662),#1522,.F.);
#24639=ADVANCED_FACE('',(#2780),#527,.T.);
#24640=ADVANCED_FACE('',(#2781),#23595,.F.);
#24641=ADVANCED_FACE('',(#2782),#528,.F.);
#24642=ADVANCED_FACE('',(#2783),#23596,.F.);
#24643=ADVANCED_FACE('',(#2784,#663,#664),#1523,.T.);
#24644=ADVANCED_FACE('',(#2785),#23597,.F.);
#24645=ADVANCED_FACE('',(#2786),#529,.F.);
#24646=ADVANCED_FACE('',(#2787),#23598,.F.);
#24944=CLOSED_SHELL('',(#24629,#24630,#24631,#24632,#24633,#24634,#24635,
#24636,#24637,#24638,#24639,#24640,#24641,#24642,#24643,#24644,#24645,#24646));
#26457=AXIS2_PLACEMENT_3D('',#40245,#32034,#32035);
#26458=AXIS2_PLACEMENT_3D('',#40246,#32036,#32037);
#26459=AXIS2_PLACEMENT_3D('',#40251,#32039,#32040);
#26460=AXIS2_PLACEMENT_3D('',#40258,#32042,#32043);
#26461=AXIS2_PLACEMENT_3D('',#40260,#32044,#32045);
#26462=AXIS2_PLACEMENT_3D('',#40262,#32046,#32047);
#26463=AXIS2_PLACEMENT_3D('',#40267,#32048,#32049);
#26464=AXIS2_PLACEMENT_3D('',#40271,#32051,#32052);
#26465=AXIS2_PLACEMENT_3D('',#40273,#32054,#32055);
#26466=AXIS2_PLACEMENT_3D('',#40279,#32059,#32060);
#26467=AXIS2_PLACEMENT_3D('',#40282,#32062,#32063);
#26468=AXIS2_PLACEMENT_3D('',#40283,#32064,#32065);
#26469=AXIS2_PLACEMENT_3D('',#40287,#32068,#32069);
#26470=AXIS2_PLACEMENT_3D('',#40289,#32070,#32071);
#26471=AXIS2_PLACEMENT_3D('',#40296,#32073,#32074);
#26472=AXIS2_PLACEMENT_3D('',#40298,#32075,#32076);
#26473=AXIS2_PLACEMENT_3D('',#40303,#32077,#32078);
#26474=AXIS2_PLACEMENT_3D('',#40306,#32080,#32081);
#26475=AXIS2_PLACEMENT_3D('',#40307,#32082,#32083);
#26476=AXIS2_PLACEMENT_3D('',#40308,#32084,#32085);
#26477=AXIS2_PLACEMENT_3D('',#40310,#32086,#32087);
#26478=AXIS2_PLACEMENT_3D('',#40312,#32088,#32089);
#26479=AXIS2_PLACEMENT_3D('',#40313,#32090,#32091);
#26480=AXIS2_PLACEMENT_3D('',#40314,#32092,#32093);
#26481=AXIS2_PLACEMENT_3D('',#40315,#32094,#32095);
#26482=AXIS2_PLACEMENT_3D('',#40318,#32097,#32098);
#26483=AXIS2_PLACEMENT_3D('',#40319,#32099,#32100);
#26484=AXIS2_PLACEMENT_3D('',#40322,#32102,#32103);
#26485=AXIS2_PLACEMENT_3D('',#40323,#32104,#32105);
#26486=AXIS2_PLACEMENT_3D('',#40325,#32106,#32107);
#26487=AXIS2_PLACEMENT_3D('',#40327,#32109,#32110);
#26488=AXIS2_PLACEMENT_3D('',#40329,#32111,#32112);
#26489=AXIS2_PLACEMENT_3D('',#40330,#32113,#32114);
#26490=AXIS2_PLACEMENT_3D('',#40333,#32116,#32117);
#26491=AXIS2_PLACEMENT_3D('',#40334,#32118,#32119);
#26492=AXIS2_PLACEMENT_3D('',#40337,#32121,#32122);
#26493=AXIS2_PLACEMENT_3D('',#40338,#32123,#32124);
#32034=DIRECTION('axis',(0.,0.,1.));
#32035=DIRECTION('refdir',(1.,0.,0.));
#32036=DIRECTION('center_axis',(0.707106781186548,0.707106781186547,0.));
#32037=DIRECTION('ref_axis',(0.,0.,-1.));
#32038=DIRECTION('',(0.,0.,1.));
#32039=DIRECTION('center_axis',(0.707106781186548,0.707106781186547,0.));
#32040=DIRECTION('ref_axis',(0.707106781186547,-0.707106781186548,5.34045053974073E-17));
#32041=DIRECTION('',(0.,0.,-1.));
#32042=DIRECTION('center_axis',(1.,0.,0.));
#32043=DIRECTION('ref_axis',(0.,0.245901639344262,-0.969294786825868));
#32044=DIRECTION('center_axis',(-1.,0.,0.));
#32045=DIRECTION('ref_axis',(0.,0.245901639344262,-0.969294786825868));
#32046=DIRECTION('center_axis',(1.,0.,0.));
#32047=DIRECTION('ref_axis',(0.,0.245901639344262,-0.969294786825868));
#32048=DIRECTION('center_axis',(0.707106781186548,-0.707106781186547,0.));
#32049=DIRECTION('ref_axis',(0.,0.,-1.));
#32050=DIRECTION('',(0.,0.,1.));
#32051=DIRECTION('center_axis',(0.707106781186548,-0.707106781186547,0.));
#32052=DIRECTION('ref_axis',(-0.707106781186547,-0.707106781186548,5.34045053974073E-17));
#32053=DIRECTION('',(0.,0.,-1.));
#32054=DIRECTION('center_axis',(0.,1.,0.));
#32055=DIRECTION('ref_axis',(0.,0.,1.));
#32056=DIRECTION('',(1.,0.,0.));
#32057=DIRECTION('',(0.,0.,-1.));
#32058=DIRECTION('',(1.,0.,0.));
#32059=DIRECTION('center_axis',(1.,0.,0.));
#32060=DIRECTION('ref_axis',(0.,-1.36502830896536E-16,-1.));
#32061=DIRECTION('',(1.,0.,0.));
#32062=DIRECTION('center_axis',(1.,0.,0.));
#32063=DIRECTION('ref_axis',(0.,0.245901639344262,-0.969294786825868));
#32064=DIRECTION('center_axis',(0.,-1.,0.));
#32065=DIRECTION('ref_axis',(0.,0.,-1.));
#32066=DIRECTION('',(1.,0.,0.));
#32067=DIRECTION('',(0.,0.,1.));
#32068=DIRECTION('center_axis',(-0.707106781186548,-0.707106781186547,0.));
#32069=DIRECTION('ref_axis',(0.,0.,1.));
#32070=DIRECTION('center_axis',(-0.707106781186548,-0.707106781186547,0.));
#32071=DIRECTION('ref_axis',(0.707106781186547,-0.707106781186548,5.34045053974073E-17));
#32072=DIRECTION('',(0.,0.,-1.));
#32073=DIRECTION('center_axis',(-1.,0.,0.));
#32074=DIRECTION('ref_axis',(0.,0.245901639344262,-0.969294786825868));
#32075=DIRECTION('center_axis',(-1.,0.,0.));
#32076=DIRECTION('ref_axis',(0.,0.245901639344262,-0.969294786825868));
#32077=DIRECTION('center_axis',(-0.707106781186548,0.707106781186547,0.));
#32078=DIRECTION('ref_axis',(0.,0.,1.));
#32079=DIRECTION('',(0.,0.,1.));
#32080=DIRECTION('center_axis',(-0.707106781186548,0.707106781186547,0.));
#32081=DIRECTION('ref_axis',(-0.707106781186547,-0.707106781186548,5.34045053974073E-17));
#32082=DIRECTION('center_axis',(1.,0.,0.));
#32083=DIRECTION('ref_axis',(0.,0.,-1.));
#32084=DIRECTION('center_axis',(1.,0.,0.));
#32085=DIRECTION('ref_axis',(0.,-0.204081632653062,0.978953873894813));
#32086=DIRECTION('center_axis',(-1.,0.,0.));
#32087=DIRECTION('ref_axis',(0.,0.,-1.));
#32088=DIRECTION('center_axis',(-1.,0.,0.));
#32089=DIRECTION('ref_axis',(0.,0.,-1.));
#32090=DIRECTION('center_axis',(1.,0.,0.));
#32091=DIRECTION('ref_axis',(0.,9.44067197810507E-16,-1.));
#32092=DIRECTION('center_axis',(1.,0.,0.));
#32093=DIRECTION('ref_axis',(0.,-0.204081632653062,0.978953873894813));
#32094=DIRECTION('center_axis',(-1.,0.,0.));
#32095=DIRECTION('ref_axis',(0.,0.,-1.));
#32096=DIRECTION('',(0.707106781186547,-8.65956056235494E-17,-0.707106781186548));
#32097=DIRECTION('center_axis',(1.,0.,0.));
#32098=DIRECTION('ref_axis',(0.,0.,-1.));
#32099=DIRECTION('center_axis',(1.,0.,0.));
#32100=DIRECTION('ref_axis',(0.,0.,-1.));
#32101=DIRECTION('',(1.,0.,0.));
#32102=DIRECTION('center_axis',(-1.,0.,0.));
#32103=DIRECTION('ref_axis',(0.,0.,-1.));
#32104=DIRECTION('center_axis',(1.,0.,0.));
#32105=DIRECTION('ref_axis',(0.,0.,-1.));
#32106=DIRECTION('center_axis',(1.,0.,0.));
#32107=DIRECTION('ref_axis',(0.,0.,-1.));
#32108=DIRECTION('',(-0.707106781186547,8.65956056235494E-17,-0.707106781186548));
#32109=DIRECTION('center_axis',(1.,0.,0.));
#32110=DIRECTION('ref_axis',(0.,0.,-1.));
#32111=DIRECTION('center_axis',(1.,0.,0.));
#32112=DIRECTION('ref_axis',(0.,0.,-1.));
#32113=DIRECTION('center_axis',(-1.,0.,0.));
#32114=DIRECTION('ref_axis',(0.,0.,-1.));
#32115=DIRECTION('',(0.707106781186547,-8.65956056235494E-17,-0.707106781186548));
#32116=DIRECTION('center_axis',(1.,0.,0.));
#32117=DIRECTION('ref_axis',(0.,0.,-1.));
#32118=DIRECTION('center_axis',(1.,0.,0.));
#32119=DIRECTION('ref_axis',(0.,0.,-1.));
#32120=DIRECTION('',(1.,0.,0.));
#32121=DIRECTION('center_axis',(-1.,0.,0.));
#32122=DIRECTION('ref_axis',(0.,0.,-1.));
#32123=DIRECTION('center_axis',(1.,0.,0.));
#32124=DIRECTION('ref_axis',(0.,0.,-1.));
#32125=DIRECTION('',(-0.707106781186547,8.65956056235494E-17,-0.707106781186548));
#40245=CARTESIAN_POINT('',(0.,0.,0.));
#40246=CARTESIAN_POINT('Origin',(1.1,-3.1,5.83535368620123));
#40247=CARTESIAN_POINT('',(1.,-3.,11.8253963992756));
#40248=CARTESIAN_POINT('',(1.,-3.,14.3906219462537));
#40249=CARTESIAN_POINT('',(1.,-3.,5.83535368620123));
#40250=CARTESIAN_POINT('',(1.2,-3.2,14.3474736452102));
#40251=CARTESIAN_POINT('Origin',(-2.00000000000001,1.08246744900953E-14,
1.38777878078145E-16));
#40252=CARTESIAN_POINT('',(1.2,-3.2,11.9799833054975));
#40253=CARTESIAN_POINT('',(1.2,-3.2,5.83535368620123));
#40254=CARTESIAN_POINT('Ctrl Pts',(1.2,-3.2,11.9799833054975));
#40255=CARTESIAN_POINT('Ctrl Pts',(1.13323634243527,-3.13323634243527,11.928712311713));
#40256=CARTESIAN_POINT('Ctrl Pts',(1.06656451099022,-3.06656451099022,11.8771826972087));
#40257=CARTESIAN_POINT('Ctrl Pts',(1.,-3.,11.8253963992756));
#40258=CARTESIAN_POINT('Origin',(1.1,-2.77555756156289E-16,-4.5102810375397E-16));
#40259=CARTESIAN_POINT('',(1.,3.,11.8253963992756));
#40260=CARTESIAN_POINT('Origin',(1.,-2.77555756156289E-16,-4.5102810375397E-16));
#40261=CARTESIAN_POINT('',(1.2,3.2,11.9799833054975));
#40262=CARTESIAN_POINT('Origin',(1.2,-2.77555756156289E-16,-4.5102810375397E-16));
#40263=CARTESIAN_POINT('Ctrl Pts',(1.2,3.2,11.9799833054975));
#40264=CARTESIAN_POINT('Ctrl Pts',(1.13323634243556,3.13323634243555,11.9287123117132));
#40265=CARTESIAN_POINT('Ctrl Pts',(1.06656451099035,3.06656451099035,11.8771826972088));
#40266=CARTESIAN_POINT('Ctrl Pts',(1.,3.,11.8253963992756));
#40267=CARTESIAN_POINT('Origin',(1.1,3.1,7.11796645969031));
#40268=CARTESIAN_POINT('',(1.2,3.2,14.3474736452102));
#40269=CARTESIAN_POINT('',(1.2,3.2,7.11796645969031));
#40270=CARTESIAN_POINT('',(1.,3.,14.3906219462537));
#40271=CARTESIAN_POINT('Origin',(-1.99999999999999,1.08246744900953E-14,
1.38777878078145E-16));
#40272=CARTESIAN_POINT('',(1.,3.,7.11796645969031));
#40273=CARTESIAN_POINT('Origin',(0.,-3.,11.8253963992756));
#40274=CARTESIAN_POINT('',(0.2,-3.,11.8253963992756));
#40275=CARTESIAN_POINT('',(0.,-3.,11.8253963992756));
#40276=CARTESIAN_POINT('',(0.2,-3.,14.3906219462537));
#40277=CARTESIAN_POINT('',(0.2,-3.,5.83535368620123));
#40278=CARTESIAN_POINT('',(0.,-3.,14.3906219462537));
#40279=CARTESIAN_POINT('Origin',(0.,-2.77555756156289E-16,-4.5102810375397E-16));
#40280=CARTESIAN_POINT('',(0.2,3.,11.8253963992756));
#40281=CARTESIAN_POINT('',(0.,3.,11.8253963992756));
#40282=CARTESIAN_POINT('Origin',(0.2,-2.77555756156289E-16,-4.5102810375397E-16));
#40283=CARTESIAN_POINT('Origin',(0.,3.,14.3906219462537));
#40284=CARTESIAN_POINT('',(0.2,3.,14.3906219462537));
#40285=CARTESIAN_POINT('',(0.,3.,14.3906219462537));
#40286=CARTESIAN_POINT('',(0.2,3.,7.11796645969031));
#40287=CARTESIAN_POINT('Origin',(0.1,3.1,7.11796645969031));
#40288=CARTESIAN_POINT('',(0.,3.2,14.3474736452102));
#40289=CARTESIAN_POINT('Origin',(3.19999999999999,1.08246744900953E-14,
1.38777878078145E-16));
#40290=CARTESIAN_POINT('',(0.,3.2,11.9799833054975));
#40291=CARTESIAN_POINT('',(0.,3.2,7.11796645969031));
#40292=CARTESIAN_POINT('Ctrl Pts',(8.15320033709099E-16,3.2,11.9799833054975));
#40293=CARTESIAN_POINT('Ctrl Pts',(0.0667636575643691,3.13323634243563,
11.9287123117132));
#40294=CARTESIAN_POINT('Ctrl Pts',(0.133435489009609,3.06656451099039,11.8771826972088));
#40295=CARTESIAN_POINT('Ctrl Pts',(0.2,3.,11.8253963992756));
#40296=CARTESIAN_POINT('Origin',(0.1,-2.77555756156289E-16,-4.5102810375397E-16));
#40297=CARTESIAN_POINT('',(0.,-3.2,11.9799833054975));
#40298=CARTESIAN_POINT('Origin',(0.,-2.77555756156289E-16,-4.5102810375397E-16));
#40299=CARTESIAN_POINT('Ctrl Pts',(-1.07552855510562E-15,-3.2,11.9799833054975));
#40300=CARTESIAN_POINT('Ctrl Pts',(0.06676365756418,-3.13323634243582,11.9287123117134));
#40301=CARTESIAN_POINT('Ctrl Pts',(0.133435489009517,-3.06656451099048,
11.8771826972089));
#40302=CARTESIAN_POINT('Ctrl Pts',(0.199999999999999,-3.,11.8253963992756));
#40303=CARTESIAN_POINT('Origin',(0.1,-3.1,5.83535368620123));
#40304=CARTESIAN_POINT('',(0.,-3.2,14.3474736452102));
#40305=CARTESIAN_POINT('',(0.,-3.2,5.83535368620123));
#40306=CARTESIAN_POINT('Origin',(3.20000000000001,1.08246744900953E-14,
1.38777878078145E-16));
#40307=CARTESIAN_POINT('Origin',(0.,1.11022302462516E-14,-0.154689026873125));
#40308=CARTESIAN_POINT('Origin',(0.,1.08246744900953E-14,1.38777878078145E-16));
#40309=CARTESIAN_POINT('',(0.,-4.5,13.67));
#40310=CARTESIAN_POINT('Origin',(0.,-4.5,12.67));
#40311=CARTESIAN_POINT('',(0.,4.5,13.67));
#40312=CARTESIAN_POINT('Origin',(0.,4.5,12.67));
#40313=CARTESIAN_POINT('Origin',(0.,1.08246744900953E-14,1.38777878078145E-16));
#40314=CARTESIAN_POINT('Origin',(1.2,1.08246744900953E-14,1.38777878078145E-16));
#40315=CARTESIAN_POINT('Origin',(0.1,-4.5,12.67));
#40316=CARTESIAN_POINT('',(0.2,-4.5,13.47));
#40317=CARTESIAN_POINT('',(0.1,-4.5,13.57));
#40318=CARTESIAN_POINT('Origin',(0.2,-4.5,12.67));
#40319=CARTESIAN_POINT('Origin',(-0.1,-4.5,12.67));
#40320=CARTESIAN_POINT('',(1.,-4.5,13.47));
#40321=CARTESIAN_POINT('',(-0.1,-4.5,13.47));
#40322=CARTESIAN_POINT('Origin',(1.,-4.5,12.67));
#40323=CARTESIAN_POINT('Origin',(1.1,-4.5,12.67));
#40324=CARTESIAN_POINT('',(1.2,-4.5,13.67));
#40325=CARTESIAN_POINT('Origin',(1.2,-4.5,12.67));
#40326=CARTESIAN_POINT('',(1.1,-4.5,13.57));
#40327=CARTESIAN_POINT('Origin',(1.2,1.11022302462516E-14,-0.154689026873125));
#40328=CARTESIAN_POINT('',(1.2,4.5,13.67));
#40329=CARTESIAN_POINT('Origin',(1.2,4.5,12.67));
#40330=CARTESIAN_POINT('Origin',(0.1,4.5,12.67));
#40331=CARTESIAN_POINT('',(0.2,4.5,13.47));
#40332=CARTESIAN_POINT('',(0.1,4.5,13.57));
#40333=CARTESIAN_POINT('Origin',(0.2,4.5,12.67));
#40334=CARTESIAN_POINT('Origin',(-0.1,4.5,12.67));
#40335=CARTESIAN_POINT('',(1.,4.5,13.47));
#40336=CARTESIAN_POINT('',(-0.1,4.5,13.47));
#40337=CARTESIAN_POINT('Origin',(1.,4.5,12.67));
#40338=CARTESIAN_POINT('Origin',(1.1,4.5,12.67));
#40339=CARTESIAN_POINT('',(1.1,4.5,13.57));
#46372=UNCERTAINTY_MEASURE_WITH_UNIT(LENGTH_MEASURE(0.01),#46396,
'DISTANCE_ACCURACY_VALUE',
'Maximum model space distance between geometric entities at asserted c
onnectivities');
#46379=UNCERTAINTY_MEASURE_WITH_UNIT(LENGTH_MEASURE(0.01),#46396,
'DISTANCE_ACCURACY_VALUE',
'Maximum model space distance between geometric entities at asserted c
onnectivities');
#46388=(
GEOMETRIC_REPRESENTATION_CONTEXT(3)
GLOBAL_UNCERTAINTY_ASSIGNED_CONTEXT((#46372))
GLOBAL_UNIT_ASSIGNED_CONTEXT((#46396,#46398,#46399))
REPRESENTATION_CONTEXT('','3D')
);
#46395=(
GEOMETRIC_REPRESENTATION_CONTEXT(3)
GLOBAL_UNCERTAINTY_ASSIGNED_CONTEXT((#46379))
GLOBAL_UNIT_ASSIGNED_CONTEXT((#46396,#46398,#46399))
REPRESENTATION_CONTEXT('','3D')
);
#46396=(
LENGTH_UNIT()
NAMED_UNIT(*)
SI_UNIT(.MILLI.,.METRE.)
);
#46398=(
NAMED_UNIT(*)
PLANE_ANGLE_UNIT()
SI_UNIT($,.RADIAN.)
);
#46399=(
NAMED_UNIT(*)
SI_UNIT($,.STERADIAN.)
SOLID_ANGLE_UNIT()
);
#46408=SHAPE_DEFINITION_REPRESENTATION(#46423,#46463);
#46423=PRODUCT_DEFINITION_SHAPE('',$,#46479);
#46463=SHAPE_REPRESENTATION('',(#26457),#46388);
#46470=PRODUCT_DEFINITION_CONTEXT('part definition',#46517,'design');
#46479=PRODUCT_DEFINITION('2026-10-26-00-51-13-699',
'09_Circlip_DIN_472_-_28',#46494,#46470);
#46494=PRODUCT_DEFINITION_FORMATION('',$,#46527);
#46517=APPLICATION_CONTEXT(
'Core Data for Automotive Mechanical Design Process');
#46518=PRODUCT_CONTEXT('part definition',#46517,'mechanical');
#46527=PRODUCT('2026-10-26-00-51-13-699','09_Circlip_DIN_472_-_28',$,(#46518));
#46590=COLOUR_RGB('Grey',0.48,0.52,0.57);
#46591=FILL_AREA_STYLE_COLOUR('',#46590);
#46592=FILL_AREA_STYLE('',(#46591));
#46593=SURFACE_STYLE_FILL_AREA(#46592);
#46594=SURFACE_SIDE_STYLE('',(#46593));
#46595=SURFACE_STYLE_USAGE(.BOTH.,#46594);
#46596=PRESENTATION_STYLE_ASSIGNMENT((#46595));
ENDSEC;
END-ISO-10303-21;
